ISO-10303-21;
HEADER;
/* Generated by software containing ST-Developer
 * from STEP Tools, Inc. (www.steptools.com) 
 */

FILE_DESCRIPTION(
/* description */ ('Jaw-coupled motor to shaft test stand'),
/* implementation_level */ '2;1');

FILE_NAME(
/* name */ 'M8x25 Bolt.step',
/* time_stamp */ '2026-10-27T10:46:06-07:00',
/* author */ (''),
/* organization */ (''),
/* preprocessor_version */ 'ST-DEVELOPER v20.2',
/* originating_system */ 'Autodesk Translation Framework v15.17.0.0',
/* authorisation */ '');

FILE_SCHEMA (('AUTOMOTIVE_DESIGN { 1 0 10303 214 3 1 1 }'));
ENDSEC;

DATA;
#10=MECHANICAL_DESIGN_GEOMETRIC_PRESENTATION_REPRESENTATION('',(#357),#19361);
#11=CONICAL_SURFACE('',#11682,0.625,0.785398163397448);
#12=CONICAL_SURFACE('',#11686,0.635,0.785398163397449);
#13=CONICAL_SURFACE('',#11690,0.41,0.463647609000806);
#29=ORIENTED_CLOSED_SHELL('',*,#11001,.F.);
#32=BREP_WITH_VOIDS('Body1',#11002,(#29));
#292=SHAPE_REPRESENTATION_RELATIONSHIP('SRR','None',#19507,#324);
#324=ADVANCED_BREP_SHAPE_REPRESENTATION('',(#32),#19343);
#357=STYLED_ITEM('',(#19753),#32);
#481=FACE_BOUND('',#1903,.T.);
#630=PLANE('',#11670);
#631=PLANE('',#11671);
#632=PLANE('',#11672);
#633=PLANE('',#11673);
#634=PLANE('',#11674);
#635=PLANE('',#11675);
#636=PLANE('',#11676);
#637=PLANE('',#11677);
#638=PLANE('',#11678);
#639=PLANE('',#11680);
#640=PLANE('',#11688);
#1191=FACE_OUTER_BOUND('',#1889,.T.);
#1192=FACE_OUTER_BOUND('',#1890,.T.);
#1193=FACE_OUTER_BOUND('',#1891,.T.);
#1194=FACE_OUTER_BOUND('',#1892,.T.);
#1195=FACE_OUTER_BOUND('',#1893,.T.);
#1196=FACE_OUTER_BOUND('',#1894,.T.);
#1197=FACE_OUTER_BOUND('',#1895,.T.);
#1198=FACE_OUTER_BOUND('',#1896,.T.);
#1199=FACE_OUTER_BOUND('',#1897,.T.);
#1200=FACE_OUTER_BOUND('',#1898,.T.);
#1201=FACE_OUTER_BOUND('',#1899,.T.);
#1202=FACE_OUTER_BOUND('',#1900,.T.);
#1203=FACE_OUTER_BOUND('',#1901,.T.);
#1204=FACE_OUTER_BOUND('',#1902,.T.);
#1205=FACE_OUTER_BOUND('',#1904,.T.);
#1206=FACE_OUTER_BOUND('',#1905,.T.);
#1889=EDGE_LOOP('',(#8092,#8093,#8094,#8095));
#1890=EDGE_LOOP('',(#8096,#8097,#8098,#8099));
#1891=EDGE_LOOP('',(#8100,#8101,#8102,#8103));
#1892=EDGE_LOOP('',(#8104,#8105,#8106,#8107));
#1893=EDGE_LOOP('',(#8108,#8109,#8110,#8111));
#1894=EDGE_LOOP('',(#8112,#8113,#8114,#8115));
#1895=EDGE_LOOP('',(#8116,#8117,#8118,#8119,#8120,#8121));
#1896=EDGE_LOOP('',(#8122,#8123,#8124,#8125,#8126,#8127));
#1897=EDGE_LOOP('',(#8128));
#1898=EDGE_LOOP('',(#8129));
#1899=EDGE_LOOP('',(#8130,#8131,#8132,#8133));
#1900=EDGE_LOOP('',(#8134,#8135,#8136,#8137));
#1901=EDGE_LOOP('',(#8138,#8139,#8140,#8141));
#1902=EDGE_LOOP('',(#8142));
#1903=EDGE_LOOP('',(#8143));
#1904=EDGE_LOOP('',(#8144,#8145,#8146,#8147));
#1905=EDGE_LOOP('',(#8148,#8149,#8150,#8151));
#2618=LINE('',#16658,#3771);
#2619=LINE('',#16660,#3772);
#2620=LINE('',#16662,#3773);
#2621=LINE('',#16663,#3774);
#2622=LINE('',#16666,#3775);
#2623=LINE('',#16668,#3776);
#2624=LINE('',#16669,#3777);
#2625=LINE('',#16672,#3778);
#2626=LINE('',#16674,#3779);
#2627=LINE('',#16675,#3780);
#2628=LINE('',#16678,#3781);
#2629=LINE('',#16680,#3782);
#2630=LINE('',#16681,#3783);
#2631=LINE('',#16684,#3784);
#2632=LINE('',#16686,#3785);
#2633=LINE('',#16687,#3786);
#2634=LINE('',#16689,#3787);
#2635=LINE('',#16690,#3788);
#2636=LINE('',#16702,#3789);
#2637=LINE('',#16706,#3790);
#2638=LINE('',#16710,#3791);
#2639=LINE('',#16717,#3792);
#2640=LINE('',#16719,#3793);
#3771=VECTOR('',#13179,1.);
#3772=VECTOR('',#13180,1.);
#3773=VECTOR('',#13181,1.);
#3774=VECTOR('',#13182,1.);
#3775=VECTOR('',#13185,1.);
#3776=VECTOR('',#13186,1.);
#3777=VECTOR('',#13187,1.);
#3778=VECTOR('',#13190,1.);
#3779=VECTOR('',#13191,1.);
#3780=VECTOR('',#13192,1.);
#3781=VECTOR('',#13195,1.);
#3782=VECTOR('',#13196,1.);
#3783=VECTOR('',#13197,1.);
#3784=VECTOR('',#13200,1.);
#3785=VECTOR('',#13201,1.);
#3786=VECTOR('',#13202,1.);
#3787=VECTOR('',#13205,1.);
#3788=VECTOR('',#13206,1.);
#3789=VECTOR('',#13223,0.625);
#3790=VECTOR('',#13228,0.65);
#3791=VECTOR('',#13233,0.635);
#3792=VECTOR('',#13242,0.41);
#3793=VECTOR('',#13245,0.4);
#4787=CIRCLE('',#11679,0.3933);
#4788=CIRCLE('',#11681,0.6);
#4789=CIRCLE('',#11683,0.65);
#4790=CIRCLE('',#11685,0.65);
#4791=CIRCLE('',#11687,0.62);
#4792=CIRCLE('',#11689,0.42);
#4793=CIRCLE('',#11691,0.3933);
#5199=VERTEX_POINT('',#16656);
#5200=VERTEX_POINT('',#16657);
#5201=VERTEX_POINT('',#16659);
#5202=VERTEX_POINT('',#16661);
#5203=VERTEX_POINT('',#16665);
#5204=VERTEX_POINT('',#16667);
#5205=VERTEX_POINT('',#16671);
#5206=VERTEX_POINT('',#16673);
#5207=VERTEX_POINT('',#16677);
#5208=VERTEX_POINT('',#16679);
#5209=VERTEX_POINT('',#16683);
#5210=VERTEX_POINT('',#16685);
#5211=VERTEX_POINT('',#16694);
#5212=VERTEX_POINT('',#16697);
#5213=VERTEX_POINT('',#16700);
#5214=VERTEX_POINT('',#16704);
#5215=VERTEX_POINT('',#16708);
#5216=VERTEX_POINT('',#16712);
#5217=VERTEX_POINT('',#16715);
#6257=EDGE_CURVE('',#5199,#5200,#2618,.T.);
#6258=EDGE_CURVE('',#5200,#5201,#2619,.T.);
#6259=EDGE_CURVE('',#5201,#5202,#2620,.T.);
#6260=EDGE_CURVE('',#5199,#5202,#2621,.T.);
#6261=EDGE_CURVE('',#5200,#5203,#2622,.T.);
#6262=EDGE_CURVE('',#5203,#5204,#2623,.T.);
#6263=EDGE_CURVE('',#5204,#5201,#2624,.T.);
#6264=EDGE_CURVE('',#5203,#5205,#2625,.T.);
#6265=EDGE_CURVE('',#5205,#5206,#2626,.T.);
#6266=EDGE_CURVE('',#5206,#5204,#2627,.T.);
#6267=EDGE_CURVE('',#5205,#5207,#2628,.T.);
#6268=EDGE_CURVE('',#5207,#5208,#2629,.T.);
#6269=EDGE_CURVE('',#5208,#5206,#2630,.T.);
#6270=EDGE_CURVE('',#5207,#5209,#2631,.T.);
#6271=EDGE_CURVE('',#5209,#5210,#2632,.T.);
#6272=EDGE_CURVE('',#5210,#5208,#2633,.T.);
#6273=EDGE_CURVE('',#5209,#5199,#2634,.T.);
#6274=EDGE_CURVE('',#5202,#5210,#2635,.T.);
#6275=EDGE_CURVE('',#5211,#5211,#4787,.T.);
#6276=EDGE_CURVE('',#5212,#5212,#4788,.T.);
#6277=EDGE_CURVE('',#5213,#5213,#4789,.T.);
#6278=EDGE_CURVE('',#5213,#5212,#2636,.T.);
#6279=EDGE_CURVE('',#5214,#5214,#4790,.T.);
#6280=EDGE_CURVE('',#5214,#5213,#2637,.T.);
#6281=EDGE_CURVE('',#5215,#5215,#4791,.T.);
#6282=EDGE_CURVE('',#5215,#5214,#2638,.T.);
#6283=EDGE_CURVE('',#5216,#5216,#4792,.T.);
#6284=EDGE_CURVE('',#5217,#5217,#4793,.F.);
#6285=EDGE_CURVE('',#5217,#5216,#2639,.T.);
#6286=EDGE_CURVE('',#5211,#5217,#2640,.T.);
#8092=ORIENTED_EDGE('',*,*,#6257,.T.);
#8093=ORIENTED_EDGE('',*,*,#6258,.T.);
#8094=ORIENTED_EDGE('',*,*,#6259,.T.);
#8095=ORIENTED_EDGE('',*,*,#6260,.F.);
#8096=ORIENTED_EDGE('',*,*,#6261,.T.);
#8097=ORIENTED_EDGE('',*,*,#6262,.T.);
#8098=ORIENTED_EDGE('',*,*,#6263,.T.);
#8099=ORIENTED_EDGE('',*,*,#6258,.F.);
#8100=ORIENTED_EDGE('',*,*,#6264,.T.);
#8101=ORIENTED_EDGE('',*,*,#6265,.T.);
#8102=ORIENTED_EDGE('',*,*,#6266,.T.);
#8103=ORIENTED_EDGE('',*,*,#6262,.F.);
#8104=ORIENTED_EDGE('',*,*,#6267,.T.);
#8105=ORIENTED_EDGE('',*,*,#6268,.T.);
#8106=ORIENTED_EDGE('',*,*,#6269,.T.);
#8107=ORIENTED_EDGE('',*,*,#6265,.F.);
#8108=ORIENTED_EDGE('',*,*,#6270,.T.);
#8109=ORIENTED_EDGE('',*,*,#6271,.T.);
#8110=ORIENTED_EDGE('',*,*,#6272,.T.);
#8111=ORIENTED_EDGE('',*,*,#6268,.F.);
#8112=ORIENTED_EDGE('',*,*,#6273,.T.);
#8113=ORIENTED_EDGE('',*,*,#6260,.T.);
#8114=ORIENTED_EDGE('',*,*,#6274,.T.);
#8115=ORIENTED_EDGE('',*,*,#6271,.F.);
#8116=ORIENTED_EDGE('',*,*,#6273,.F.);
#8117=ORIENTED_EDGE('',*,*,#6270,.F.);
#8118=ORIENTED_EDGE('',*,*,#6267,.F.);
#8119=ORIENTED_EDGE('',*,*,#6264,.F.);
#8120=ORIENTED_EDGE('',*,*,#6261,.F.);
#8121=ORIENTED_EDGE('',*,*,#6257,.F.);
#8122=ORIENTED_EDGE('',*,*,#6274,.F.);
#8123=ORIENTED_EDGE('',*,*,#6259,.F.);
#8124=ORIENTED_EDGE('',*,*,#6263,.F.);
#8125=ORIENTED_EDGE('',*,*,#6266,.F.);
#8126=ORIENTED_EDGE('',*,*,#6269,.F.);
#8127=ORIENTED_EDGE('',*,*,#6272,.F.);
#8128=ORIENTED_EDGE('',*,*,#6275,.F.);
#8129=ORIENTED_EDGE('',*,*,#6276,.F.);
#8130=ORIENTED_EDGE('',*,*,#6277,.F.);
#8131=ORIENTED_EDGE('',*,*,#6278,.T.);
#8132=ORIENTED_EDGE('',*,*,#6276,.T.);
#8133=ORIENTED_EDGE('',*,*,#6278,.F.);
#8134=ORIENTED_EDGE('',*,*,#6279,.F.);
#8135=ORIENTED_EDGE('',*,*,#6280,.T.);
#8136=ORIENTED_EDGE('',*,*,#6277,.T.);
#8137=ORIENTED_EDGE('',*,*,#6280,.F.);
#8138=ORIENTED_EDGE('',*,*,#6281,.F.);
#8139=ORIENTED_EDGE('',*,*,#6282,.T.);
#8140=ORIENTED_EDGE('',*,*,#6279,.T.);
#8141=ORIENTED_EDGE('',*,*,#6282,.F.);
#8142=ORIENTED_EDGE('',*,*,#6281,.T.);
#8143=ORIENTED_EDGE('',*,*,#6283,.F.);
#8144=ORIENTED_EDGE('',*,*,#6284,.F.);
#8145=ORIENTED_EDGE('',*,*,#6285,.T.);
#8146=ORIENTED_EDGE('',*,*,#6283,.T.);
#8147=ORIENTED_EDGE('',*,*,#6285,.F.);
#8148=ORIENTED_EDGE('',*,*,#6275,.T.);
#8149=ORIENTED_EDGE('',*,*,#6286,.T.);
#8150=ORIENTED_EDGE('',*,*,#6284,.T.);
#8151=ORIENTED_EDGE('',*,*,#6286,.F.);
#10323=CYLINDRICAL_SURFACE('',#11684,0.65);
#10324=CYLINDRICAL_SURFACE('',#11692,0.3933);
#10533=ADVANCED_FACE('',(#1191),#630,.F.);
#10534=ADVANCED_FACE('',(#1192),#631,.F.);
#10535=ADVANCED_FACE('',(#1193),#632,.F.);
#10536=ADVANCED_FACE('',(#1194),#633,.F.);
#10537=ADVANCED_FACE('',(#1195),#634,.F.);
#10538=ADVANCED_FACE('',(#1196),#635,.F.);
#10539=ADVANCED_FACE('',(#1197),#636,.F.);
#10540=ADVANCED_FACE('',(#1198),#637,.F.);
#10541=ADVANCED_FACE('',(#1199),#638,.F.);
#10542=ADVANCED_FACE('',(#1200),#639,.T.);
#10543=ADVANCED_FACE('',(#1201),#11,.T.);
#10544=ADVANCED_FACE('',(#1202),#10323,.T.);
#10545=ADVANCED_FACE('',(#1203),#12,.T.);
#10546=ADVANCED_FACE('',(#1204,#481),#640,.T.);
#10547=ADVANCED_FACE('',(#1205),#13,.T.);
#10548=ADVANCED_FACE('',(#1206),#10324,.T.);
#11001=CLOSED_SHELL('',(#10533,#10534,#10535,#10536,#10537,#10538,#10539,
#10540));
#11002=CLOSED_SHELL('',(#10541,#10542,#10543,#10544,#10545,#10546,#10547,
#10548));
#11669=AXIS2_PLACEMENT_3D('',#16654,#13175,#13176);
#11670=AXIS2_PLACEMENT_3D('',#16655,#13177,#13178);
#11671=AXIS2_PLACEMENT_3D('',#16664,#13183,#13184);
#11672=AXIS2_PLACEMENT_3D('',#16670,#13188,#13189);
#11673=AXIS2_PLACEMENT_3D('',#16676,#13193,#13194);
#11674=AXIS2_PLACEMENT_3D('',#16682,#13198,#13199);
#11675=AXIS2_PLACEMENT_3D('',#16688,#13203,#13204);
#11676=AXIS2_PLACEMENT_3D('',#16691,#13207,#13208);
#11677=AXIS2_PLACEMENT_3D('',#16692,#13209,#13210);
#11678=AXIS2_PLACEMENT_3D('',#16693,#13211,#13212);
#11679=AXIS2_PLACEMENT_3D('',#16695,#13213,#13214);
#11680=AXIS2_PLACEMENT_3D('',#16696,#13215,#13216);
#11681=AXIS2_PLACEMENT_3D('',#16698,#13217,#13218);
#11682=AXIS2_PLACEMENT_3D('',#16699,#13219,#13220);
#11683=AXIS2_PLACEMENT_3D('',#16701,#13221,#13222);
#11684=AXIS2_PLACEMENT_3D('',#16703,#13224,#13225);
#11685=AXIS2_PLACEMENT_3D('',#16705,#13226,#13227);
#11686=AXIS2_PLACEMENT_3D('',#16707,#13229,#13230);
#11687=AXIS2_PLACEMENT_3D('',#16709,#13231,#13232);
#11688=AXIS2_PLACEMENT_3D('',#16711,#13234,#13235);
#11689=AXIS2_PLACEMENT_3D('',#16713,#13236,#13237);
#11690=AXIS2_PLACEMENT_3D('',#16714,#13238,#13239);
#11691=AXIS2_PLACEMENT_3D('',#16716,#13240,#13241);
#11692=AXIS2_PLACEMENT_3D('',#16718,#13243,#13244);
#13175=DIRECTION('axis',(0.,0.,1.));
#13176=DIRECTION('refdir',(1.,0.,0.));
#13177=DIRECTION('center_axis',(0.866025403784439,0.,-0.5));
#13178=DIRECTION('ref_axis',(0.5,0.,0.866025403784439));
#13179=DIRECTION('',(-0.5,0.,-0.866025403784439));
#13180=DIRECTION('',(0.,-1.,0.));
#13181=DIRECTION('',(0.5,0.,0.866025403784439));
#13182=DIRECTION('',(0.,-1.,0.));
#13183=DIRECTION('center_axis',(1.60246890531964E-16,0.,-1.));
#13184=DIRECTION('ref_axis',(1.,0.,1.60246890531964E-16));
#13185=DIRECTION('',(-1.,0.,-1.60246890531964E-16));
#13186=DIRECTION('',(0.,-1.,0.));
#13187=DIRECTION('',(1.,0.,1.60246890531964E-16));
#13188=DIRECTION('center_axis',(-0.866025403784439,0.,-0.5));
#13189=DIRECTION('ref_axis',(0.5,0.,-0.866025403784439));
#13190=DIRECTION('',(-0.5,0.,0.866025403784439));
#13191=DIRECTION('',(0.,-1.,0.));
#13192=DIRECTION('',(0.5,0.,-0.866025403784439));
#13193=DIRECTION('center_axis',(-0.866025403784439,0.,0.5));
#13194=DIRECTION('ref_axis',(-0.5,0.,-0.866025403784439));
#13195=DIRECTION('',(0.5,0.,0.866025403784439));
#13196=DIRECTION('',(0.,-1.,0.));
#13197=DIRECTION('',(-0.5,0.,-0.866025403784439));
#13198=DIRECTION('center_axis',(-1.60246890531964E-16,0.,1.));
#13199=DIRECTION('ref_axis',(-1.,0.,-1.60246890531964E-16));
#13200=DIRECTION('',(1.,0.,1.60246890531964E-16));
#13201=DIRECTION('',(0.,-1.,0.));
#13202=DIRECTION('',(-1.,0.,-1.60246890531964E-16));
#13203=DIRECTION('center_axis',(0.866025403784439,0.,0.5));
#13204=DIRECTION('ref_axis',(-0.5,0.,0.866025403784439));
#13205=DIRECTION('',(0.5,0.,-0.866025403784439));
#13206=DIRECTION('',(-0.5,0.,0.866025403784439));
#13207=DIRECTION('center_axis',(0.,1.,0.));
#13208=DIRECTION('ref_axis',(1.,0.,0.));
#13209=DIRECTION('center_axis',(0.,-1.,0.));
#13210=DIRECTION('ref_axis',(0.,0.,-1.));
#13211=DIRECTION('center_axis',(0.,1.,0.));
#13212=DIRECTION('ref_axis',(1.,0.,0.));
#13213=DIRECTION('center_axis',(0.,1.,0.));
#13214=DIRECTION('ref_axis',(1.,0.,0.));
#13215=DIRECTION('center_axis',(0.,1.,0.));
#13216=DIRECTION('ref_axis',(0.,0.,1.));
#13217=DIRECTION('center_axis',(0.,-1.,0.));
#13218=DIRECTION('ref_axis',(1.,0.,0.));
#13219=DIRECTION('center_axis',(0.,-1.,0.));
#13220=DIRECTION('ref_axis',(1.,0.,0.));
#13221=DIRECTION('center_axis',(0.,-1.,0.));
#13222=DIRECTION('ref_axis',(1.,0.,0.));
#13223=DIRECTION('',(0.707106781186548,0.707106781186547,8.65956056235493E-17));
#13224=DIRECTION('center_axis',(0.,-1.,0.));
#13225=DIRECTION('ref_axis',(1.,0.,0.));
#13226=DIRECTION('center_axis',(0.,-1.,0.));
#13227=DIRECTION('ref_axis',(1.,0.,0.));
#13228=DIRECTION('',(0.,1.,0.));
#13229=DIRECTION('center_axis',(0.,1.,0.));
#13230=DIRECTION('ref_axis',(1.,0.,0.));
#13231=DIRECTION('center_axis',(0.,-1.,0.));
#13232=DIRECTION('ref_axis',(1.,0.,0.));
#13233=DIRECTION('',(-0.707106781186548,0.707106781186547,-8.65956056235494E-17));
#13234=DIRECTION('center_axis',(0.,-1.,0.));
#13235=DIRECTION('ref_axis',(0.,0.,-1.));
#13236=DIRECTION('center_axis',(0.,-1.,0.));
#13237=DIRECTION('ref_axis',(1.,0.,0.));
#13238=DIRECTION('center_axis',(0.,1.,0.));
#13239=DIRECTION('ref_axis',(1.,0.,0.));
#13240=DIRECTION('center_axis',(0.,1.,0.));
#13241=DIRECTION('ref_axis',(1.,0.,0.));
#13242=DIRECTION('',(-0.447213595499958,0.894427190999916,-5.47678698264203E-17));
#13243=DIRECTION('center_axis',(0.,-1.,0.));
#13244=DIRECTION('ref_axis',(1.,0.,0.));
#13245=DIRECTION('',(0.,1.,0.));
#16654=CARTESIAN_POINT('',(0.,0.,0.));
#16655=CARTESIAN_POINT('Origin',(0.173205080756888,-0.8,-0.3));
#16656=CARTESIAN_POINT('',(0.346410161513775,-0.8,0.));
#16657=CARTESIAN_POINT('',(0.173205080756888,-0.8,-0.3));
#16658=CARTESIAN_POINT('',(0.346410161513775,-0.8,0.));
#16659=CARTESIAN_POINT('',(0.173205080756888,-1.28,-0.3));
#16660=CARTESIAN_POINT('',(0.173205080756888,-0.8,-0.3));
#16661=CARTESIAN_POINT('',(0.346410161513775,-1.28,0.));
#16662=CARTESIAN_POINT('',(0.346410161513775,-1.28,0.));
#16663=CARTESIAN_POINT('',(0.346410161513775,-0.8,0.));
#16664=CARTESIAN_POINT('Origin',(-0.173205080756888,-0.8,-0.3));
#16665=CARTESIAN_POINT('',(-0.173205080756888,-0.8,-0.3));
#16666=CARTESIAN_POINT('',(0.173205080756888,-0.8,-0.3));
#16667=CARTESIAN_POINT('',(-0.173205080756888,-1.28,-0.3));
#16668=CARTESIAN_POINT('',(-0.173205080756888,-0.8,-0.3));
#16669=CARTESIAN_POINT('',(0.173205080756888,-1.28,-0.3));
#16670=CARTESIAN_POINT('Origin',(-0.346410161513775,-0.8,-5.55111512312578E-17));
#16671=CARTESIAN_POINT('',(-0.346410161513775,-0.8,-4.24230095489963E-17));
#16672=CARTESIAN_POINT('',(-0.173205080756888,-0.8,-0.3));
#16673=CARTESIAN_POINT('',(-0.346410161513775,-1.28,-5.55111512312578E-17));
#16674=CARTESIAN_POINT('',(-0.346410161513775,-0.8,-4.24230095489963E-17));
#16675=CARTESIAN_POINT('',(-0.173205080756888,-1.28,-0.3));
#16676=CARTESIAN_POINT('Origin',(-0.173205080756888,-0.8,0.3));
#16677=CARTESIAN_POINT('',(-0.173205080756888,-0.8,0.3));
#16678=CARTESIAN_POINT('',(-0.346410161513775,-0.8,-4.24230095489963E-17));
#16679=CARTESIAN_POINT('',(-0.173205080756888,-1.28,0.3));
#16680=CARTESIAN_POINT('',(-0.173205080756888,-0.8,0.3));
#16681=CARTESIAN_POINT('',(-0.346410161513775,-1.28,-4.24230095489963E-17));
#16682=CARTESIAN_POINT('Origin',(0.173205080756888,-0.8,0.3));
#16683=CARTESIAN_POINT('',(0.173205080756888,-0.8,0.3));
#16684=CARTESIAN_POINT('',(-0.173205080756888,-0.8,0.3));
#16685=CARTESIAN_POINT('',(0.173205080756888,-1.28,0.3));
#16686=CARTESIAN_POINT('',(0.173205080756888,-0.8,0.3));
#16687=CARTESIAN_POINT('',(-0.173205080756888,-1.28,0.3));
#16688=CARTESIAN_POINT('Origin',(0.346410161513775,-0.8,0.));
#16689=CARTESIAN_POINT('',(0.173205080756888,-0.8,0.3));
#16690=CARTESIAN_POINT('',(0.173205080756888,-1.28,0.3));
#16691=CARTESIAN_POINT('Origin',(0.,-0.8,-5.55111512312578E-17));
#16692=CARTESIAN_POINT('Origin',(0.,-1.28,-5.55111512312578E-17));
#16693=CARTESIAN_POINT('Origin',(0.,-2.5,0.));
#16694=CARTESIAN_POINT('',(-0.3933,-2.5,4.81653586104654E-17));
#16695=CARTESIAN_POINT('Origin',(0.,-2.5,0.));
#16696=CARTESIAN_POINT('Origin',(0.6,0.8,0.));
#16697=CARTESIAN_POINT('',(-0.6,0.8,-7.34788079488412E-17));
#16698=CARTESIAN_POINT('Origin',(0.,0.8,0.));
#16699=CARTESIAN_POINT('Origin',(0.,0.775,0.));
#16700=CARTESIAN_POINT('',(-0.65,0.75,-7.9602041944578E-17));
#16701=CARTESIAN_POINT('Origin',(0.,0.75,0.));
#16702=CARTESIAN_POINT('',(-0.625,0.775,-7.65404249467096E-17));
#16703=CARTESIAN_POINT('Origin',(0.,0.39,0.));
#16704=CARTESIAN_POINT('',(-0.65,0.0299999999999998,-7.9602041944578E-17));
#16705=CARTESIAN_POINT('Origin',(0.,0.0299999999999998,0.));
#16706=CARTESIAN_POINT('',(-0.65,0.39,-7.9602041944578E-17));
#16707=CARTESIAN_POINT('Origin',(0.,0.0150000000000001,0.));
#16708=CARTESIAN_POINT('',(-0.62,5.89805981832114E-17,-7.59281015471359E-17));
#16709=CARTESIAN_POINT('Origin',(0.,0.,0.));
#16710=CARTESIAN_POINT('',(-0.635,0.0150000000000001,-7.77650717458569E-17));
#16711=CARTESIAN_POINT('Origin',(0.42,0.,0.));
#16712=CARTESIAN_POINT('',(-0.42,-3.46944695195361E-18,-5.14351655641888E-17));
#16713=CARTESIAN_POINT('Origin',(0.,0.,0.));
#16714=CARTESIAN_POINT('Origin',(0.,-0.02,0.));
#16715=CARTESIAN_POINT('',(-0.3933,-0.0534000000000001,4.81653586104654E-17));
#16716=CARTESIAN_POINT('Origin',(0.,-0.0534000000000001,0.));
#16717=CARTESIAN_POINT('',(-0.41,-0.02,-5.02105187650415E-17));
#16718=CARTESIAN_POINT('Origin',(0.,-1.48,0.));
#16719=CARTESIAN_POINT('',(-0.3933,-1.48,-4.81653586104654E-17));
#19305=UNCERTAINTY_MEASURE_WITH_UNIT(LENGTH_MEASURE(0.001),#19362,
'DISTANCE_ACCURACY_VALUE',
'Maximum model space distance between geometric entities at asserted c
onnectivities');
#19323=UNCERTAINTY_MEASURE_WITH_UNIT(LENGTH_MEASURE(0.001),#19362,
'DISTANCE_ACCURACY_VALUE',
'Maximum model space distance between geometric entities at asserted c
onnectivities');
#19343=(
GEOMETRIC_REPRESENTATION_CONTEXT(3)
GLOBAL_UNCERTAINTY_ASSIGNED_CONTEXT((#19305))
GLOBAL_UNIT_ASSIGNED_CONTEXT((#19362,#19364,#19365))
REPRESENTATION_CONTEXT('','3D')
);
#19361=(
GEOMETRIC_REPRESENTATION_CONTEXT(3)
GLOBAL_UNCERTAINTY_ASSIGNED_CONTEXT((#19323))
GLOBAL_UNIT_ASSIGNED_CONTEXT((#19362,#19364,#19365))
REPRESENTATION_CONTEXT('','3D')
);
#19362=(
LENGTH_UNIT()
NAMED_UNIT(*)
SI_UNIT(.CENTI.,.METRE.)
);
#19364=(
NAMED_UNIT(*)
PLANE_ANGLE_UNIT()
SI_UNIT($,.RADIAN.)
);
#19365=(
NAMED_UNIT(*)
SI_UNIT($,.STERADIAN.)
SOLID_ANGLE_UNIT()
);
#19385=SHAPE_DEFINITION_REPRESENTATION(#19424,#19507);
#19424=PRODUCT_DEFINITION_SHAPE('',$,#19545);
#19507=SHAPE_REPRESENTATION('',(#11669),#19343);
#19525=PRODUCT_DEFINITION_CONTEXT('part definition',#19638,'design');
#19545=PRODUCT_DEFINITION('M8x25 Bolt','M8x25 Bolt',#19582,#19525);
#19582=PRODUCT_DEFINITION_FORMATION('',$,#19659);
#19638=APPLICATION_CONTEXT(
'Core Data for Automotive Mechanical Design Process');
#19639=PRODUCT_CONTEXT('part definition',#19638,'mechanical');
#19659=PRODUCT('M8x25 Bolt','M8x25 Bolt','M8x25 Bolt',(#19639));
#19747=COLOUR_RGB('Black',0.12,0.14,0.17);
#19748=FILL_AREA_STYLE_COLOUR('',#19747);
#19749=FILL_AREA_STYLE('',(#19748));
#19750=SURFACE_STYLE_FILL_AREA(#19749);
#19751=SURFACE_SIDE_STYLE('',(#19750));
#19752=SURFACE_STYLE_USAGE(.BOTH.,#19751);
#19753=PRESENTATION_STYLE_ASSIGNMENT((#19752));
ENDSEC;
END-ISO-10303-21;
